ISO-10303-21;
HEADER;
/* Generated by software containing ST-Developer
 * from STEP Tools, Inc. (www.steptools.com) 
 */

FILE_DESCRIPTION(
/* description */ ('Bearing friction torque test rig'),
/* implementation_level */ '2;1');

FILE_NAME(
/* name */ 'Socket Set Screw - M5x8.step',
/* time_stamp */ '2026-10-28T03:24:04-07:00',
/* author */ (''),
/* organization */ (''),
/* preprocessor_version */ 'ST-DEVELOPER v20.2',
/* originating_system */ 'Autodesk Translation Framework v15.17.0.0',
/* authorisation */ '');

FILE_SCHEMA (('AUTOMOTIVE_DESIGN { 1 0 10303 214 3 1 1 }'));
ENDSEC;

DATA;
#10=MECHANICAL_DESIGN_GEOMETRIC_PRESENTATION_REPRESENTATION('',(#592),#14822);
#447=CONICAL_SURFACE('',#9142,0.235,0.785398163397448);
#448=CONICAL_SURFACE('',#9146,0.2125,0.785398163397448);
#499=SHAPE_REPRESENTATION_RELATIONSHIP('SRR','None',#15041,#538);
#538=ADVANCED_BREP_SHAPE_REPRESENTATION('',(#643),#14821);
#592=STYLED_ITEM('',(#15291),#643);
#643=MANIFOLD_SOLID_BREP('Body1',#7711);
#873=FACE_BOUND('',#2214,.T.);
#1090=PLANE('',#9133);
#1091=PLANE('',#9134);
#1092=PLANE('',#9135);
#1093=PLANE('',#9136);
#1094=PLANE('',#9137);
#1095=PLANE('',#9138);
#1096=PLANE('',#9139);
#1097=PLANE('',#9140);
#1098=PLANE('',#9148);
#1532=FACE_OUTER_BOUND('',#2206,.T.);
#1533=FACE_OUTER_BOUND('',#2207,.T.);
#1534=FACE_OUTER_BOUND('',#2208,.T.);
#1535=FACE_OUTER_BOUND('',#2209,.T.);
#1536=FACE_OUTER_BOUND('',#2210,.T.);
#1537=FACE_OUTER_BOUND('',#2211,.T.);
#1538=FACE_OUTER_BOUND('',#2212,.T.);
#1539=FACE_OUTER_BOUND('',#2213,.T.);
#1540=FACE_OUTER_BOUND('',#2215,.T.);
#1541=FACE_OUTER_BOUND('',#2216,.T.);
#1542=FACE_OUTER_BOUND('',#2217,.T.);
#1543=FACE_OUTER_BOUND('',#2218,.T.);
#2206=EDGE_LOOP('',(#6994,#6995,#6996,#6997));
#2207=EDGE_LOOP('',(#6998,#6999,#7000,#7001));
#2208=EDGE_LOOP('',(#7002,#7003,#7004,#7005));
#2209=EDGE_LOOP('',(#7006,#7007,#7008,#7009));
#2210=EDGE_LOOP('',(#7010,#7011,#7012,#7013));
#2211=EDGE_LOOP('',(#7014,#7015,#7016,#7017));
#2212=EDGE_LOOP('',(#7018,#7019,#7020,#7021,#7022,#7023));
#2213=EDGE_LOOP('',(#7024));
#2214=EDGE_LOOP('',(#7025,#7026,#7027,#7028,#7029,#7030));
#2215=EDGE_LOOP('',(#7031,#7032,#7033,#7034));
#2216=EDGE_LOOP('',(#7035,#7036,#7037,#7038));
#2217=EDGE_LOOP('',(#7039,#7040,#7041,#7042));
#2218=EDGE_LOOP('',(#7043));
#2642=LINE('',#14666,#3086);
#2643=LINE('',#14668,#3087);
#2644=LINE('',#14670,#3088);
#2645=LINE('',#14671,#3089);
#2646=LINE('',#14674,#3090);
#2647=LINE('',#14676,#3091);
#2648=LINE('',#14677,#3092);
#2649=LINE('',#14680,#3093);
#2650=LINE('',#14682,#3094);
#2651=LINE('',#14683,#3095);
#2652=LINE('',#14686,#3096);
#2653=LINE('',#14688,#3097);
#2654=LINE('',#14689,#3098);
#2655=LINE('',#14692,#3099);
#2656=LINE('',#14694,#3100);
#2657=LINE('',#14695,#3101);
#2658=LINE('',#14697,#3102);
#2659=LINE('',#14698,#3103);
#2660=LINE('',#14706,#3104);
#2661=LINE('',#14710,#3105);
#2662=LINE('',#14714,#3106);
#3086=VECTOR('',#11573,1.);
#3087=VECTOR('',#11574,1.);
#3088=VECTOR('',#11575,1.);
#3089=VECTOR('',#11576,1.);
#3090=VECTOR('',#11579,1.);
#3091=VECTOR('',#11580,1.);
#3092=VECTOR('',#11581,1.);
#3093=VECTOR('',#11584,1.);
#3094=VECTOR('',#11585,1.);
#3095=VECTOR('',#11586,1.);
#3096=VECTOR('',#11589,1.);
#3097=VECTOR('',#11590,1.);
#3098=VECTOR('',#11591,1.);
#3099=VECTOR('',#11594,1.);
#3100=VECTOR('',#11595,1.);
#3101=VECTOR('',#11596,1.);
#3102=VECTOR('',#11599,1.);
#3103=VECTOR('',#11600,1.);
#3104=VECTOR('',#11611,0.235);
#3105=VECTOR('',#11616,0.25);
#3106=VECTOR('',#11621,0.2125);
#3549=CIRCLE('',#9141,0.22);
#3550=CIRCLE('',#9143,0.24505);
#3551=CIRCLE('',#9145,0.24505);
#3552=CIRCLE('',#9147,0.175);
#4184=VERTEX_POINT('',#14664);
#4185=VERTEX_POINT('',#14665);
#4186=VERTEX_POINT('',#14667);
#4187=VERTEX_POINT('',#14669);
#4188=VERTEX_POINT('',#14673);
#4189=VERTEX_POINT('',#14675);
#4190=VERTEX_POINT('',#14679);
#4191=VERTEX_POINT('',#14681);
#4192=VERTEX_POINT('',#14685);
#4193=VERTEX_POINT('',#14687);
#4194=VERTEX_POINT('',#14691);
#4195=VERTEX_POINT('',#14693);
#4196=VERTEX_POINT('',#14701);
#4197=VERTEX_POINT('',#14704);
#4198=VERTEX_POINT('',#14708);
#4199=VERTEX_POINT('',#14712);
#5123=EDGE_CURVE('',#4184,#4185,#2642,.T.);
#5124=EDGE_CURVE('',#4184,#4186,#2643,.T.);
#5125=EDGE_CURVE('',#4186,#4187,#2644,.T.);
#5126=EDGE_CURVE('',#4185,#4187,#2645,.T.);
#5127=EDGE_CURVE('',#4188,#4184,#2646,.T.);
#5128=EDGE_CURVE('',#4188,#4189,#2647,.T.);
#5129=EDGE_CURVE('',#4189,#4186,#2648,.T.);
#5130=EDGE_CURVE('',#4190,#4188,#2649,.T.);
#5131=EDGE_CURVE('',#4190,#4191,#2650,.T.);
#5132=EDGE_CURVE('',#4191,#4189,#2651,.T.);
#5133=EDGE_CURVE('',#4192,#4190,#2652,.T.);
#5134=EDGE_CURVE('',#4192,#4193,#2653,.T.);
#5135=EDGE_CURVE('',#4193,#4191,#2654,.T.);
#5136=EDGE_CURVE('',#4194,#4192,#2655,.T.);
#5137=EDGE_CURVE('',#4194,#4195,#2656,.T.);
#5138=EDGE_CURVE('',#4195,#4193,#2657,.T.);
#5139=EDGE_CURVE('',#4185,#4194,#2658,.T.);
#5140=EDGE_CURVE('',#4187,#4195,#2659,.T.);
#5141=EDGE_CURVE('',#4196,#4196,#3549,.T.);
#5142=EDGE_CURVE('',#4197,#4197,#3550,.T.);
#5143=EDGE_CURVE('',#4197,#4196,#2660,.T.);
#5144=EDGE_CURVE('',#4198,#4198,#3551,.F.);
#5145=EDGE_CURVE('',#4198,#4197,#2661,.T.);
#5146=EDGE_CURVE('',#4199,#4199,#3552,.T.);
#5147=EDGE_CURVE('',#4199,#4198,#2662,.T.);
#6994=ORIENTED_EDGE('',*,*,#5123,.F.);
#6995=ORIENTED_EDGE('',*,*,#5124,.T.);
#6996=ORIENTED_EDGE('',*,*,#5125,.T.);
#6997=ORIENTED_EDGE('',*,*,#5126,.F.);
#6998=ORIENTED_EDGE('',*,*,#5127,.F.);
#6999=ORIENTED_EDGE('',*,*,#5128,.T.);
#7000=ORIENTED_EDGE('',*,*,#5129,.T.);
#7001=ORIENTED_EDGE('',*,*,#5124,.F.);
#7002=ORIENTED_EDGE('',*,*,#5130,.F.);
#7003=ORIENTED_EDGE('',*,*,#5131,.T.);
#7004=ORIENTED_EDGE('',*,*,#5132,.T.);
#7005=ORIENTED_EDGE('',*,*,#5128,.F.);
#7006=ORIENTED_EDGE('',*,*,#5133,.F.);
#7007=ORIENTED_EDGE('',*,*,#5134,.T.);
#7008=ORIENTED_EDGE('',*,*,#5135,.T.);
#7009=ORIENTED_EDGE('',*,*,#5131,.F.);
#7010=ORIENTED_EDGE('',*,*,#5136,.F.);
#7011=ORIENTED_EDGE('',*,*,#5137,.T.);
#7012=ORIENTED_EDGE('',*,*,#5138,.T.);
#7013=ORIENTED_EDGE('',*,*,#5134,.F.);
#7014=ORIENTED_EDGE('',*,*,#5139,.F.);
#7015=ORIENTED_EDGE('',*,*,#5126,.T.);
#7016=ORIENTED_EDGE('',*,*,#5140,.T.);
#7017=ORIENTED_EDGE('',*,*,#5137,.F.);
#7018=ORIENTED_EDGE('',*,*,#5140,.F.);
#7019=ORIENTED_EDGE('',*,*,#5125,.F.);
#7020=ORIENTED_EDGE('',*,*,#5129,.F.);
#7021=ORIENTED_EDGE('',*,*,#5132,.F.);
#7022=ORIENTED_EDGE('',*,*,#5135,.F.);
#7023=ORIENTED_EDGE('',*,*,#5138,.F.);
#7024=ORIENTED_EDGE('',*,*,#5141,.F.);
#7025=ORIENTED_EDGE('',*,*,#5123,.T.);
#7026=ORIENTED_EDGE('',*,*,#5139,.T.);
#7027=ORIENTED_EDGE('',*,*,#5136,.T.);
#7028=ORIENTED_EDGE('',*,*,#5133,.T.);
#7029=ORIENTED_EDGE('',*,*,#5130,.T.);
#7030=ORIENTED_EDGE('',*,*,#5127,.T.);
#7031=ORIENTED_EDGE('',*,*,#5142,.F.);
#7032=ORIENTED_EDGE('',*,*,#5143,.T.);
#7033=ORIENTED_EDGE('',*,*,#5141,.T.);
#7034=ORIENTED_EDGE('',*,*,#5143,.F.);
#7035=ORIENTED_EDGE('',*,*,#5144,.F.);
#7036=ORIENTED_EDGE('',*,*,#5145,.T.);
#7037=ORIENTED_EDGE('',*,*,#5142,.T.);
#7038=ORIENTED_EDGE('',*,*,#5145,.F.);
#7039=ORIENTED_EDGE('',*,*,#5146,.F.);
#7040=ORIENTED_EDGE('',*,*,#5147,.T.);
#7041=ORIENTED_EDGE('',*,*,#5144,.T.);
#7042=ORIENTED_EDGE('',*,*,#5147,.F.);
#7043=ORIENTED_EDGE('',*,*,#5146,.T.);
#7209=CYLINDRICAL_SURFACE('',#9144,0.24505);
#7643=ADVANCED_FACE('',(#1532),#1090,.F.);
#7644=ADVANCED_FACE('',(#1533),#1091,.F.);
#7645=ADVANCED_FACE('',(#1534),#1092,.F.);
#7646=ADVANCED_FACE('',(#1535),#1093,.F.);
#7647=ADVANCED_FACE('',(#1536),#1094,.F.);
#7648=ADVANCED_FACE('',(#1537),#1095,.F.);
#7649=ADVANCED_FACE('',(#1538),#1096,.F.);
#7650=ADVANCED_FACE('',(#1539,#873),#1097,.T.);
#7651=ADVANCED_FACE('',(#1540),#447,.T.);
#7652=ADVANCED_FACE('',(#1541),#7209,.T.);
#7653=ADVANCED_FACE('',(#1542),#448,.T.);
#7654=ADVANCED_FACE('',(#1543),#1098,.T.);
#7711=CLOSED_SHELL('',(#7643,#7644,#7645,#7646,#7647,#7648,#7649,#7650,
#7651,#7652,#7653,#7654));
#9132=AXIS2_PLACEMENT_3D('',#14662,#11569,#11570);
#9133=AXIS2_PLACEMENT_3D('',#14663,#11571,#11572);
#9134=AXIS2_PLACEMENT_3D('',#14672,#11577,#11578);
#9135=AXIS2_PLACEMENT_3D('',#14678,#11582,#11583);
#9136=AXIS2_PLACEMENT_3D('',#14684,#11587,#11588);
#9137=AXIS2_PLACEMENT_3D('',#14690,#11592,#11593);
#9138=AXIS2_PLACEMENT_3D('',#14696,#11597,#11598);
#9139=AXIS2_PLACEMENT_3D('',#14699,#11601,#11602);
#9140=AXIS2_PLACEMENT_3D('',#14700,#11603,#11604);
#9141=AXIS2_PLACEMENT_3D('',#14702,#11605,#11606);
#9142=AXIS2_PLACEMENT_3D('',#14703,#11607,#11608);
#9143=AXIS2_PLACEMENT_3D('',#14705,#11609,#11610);
#9144=AXIS2_PLACEMENT_3D('',#14707,#11612,#11613);
#9145=AXIS2_PLACEMENT_3D('',#14709,#11614,#11615);
#9146=AXIS2_PLACEMENT_3D('',#14711,#11617,#11618);
#9147=AXIS2_PLACEMENT_3D('',#14713,#11619,#11620);
#9148=AXIS2_PLACEMENT_3D('',#14715,#11622,#11623);
#11569=DIRECTION('axis',(0.,0.,1.));
#11570=DIRECTION('refdir',(1.,0.,0.));
#11571=DIRECTION('center_axis',(0.866025403784439,0.,-0.5));
#11572=DIRECTION('ref_axis',(0.5,0.,0.866025403784439));
#11573=DIRECTION('',(0.5,0.,0.866025403784439));
#11574=DIRECTION('',(0.,-1.,0.));
#11575=DIRECTION('',(0.5,0.,0.866025403784439));
#11576=DIRECTION('',(0.,-1.,0.));
#11577=DIRECTION('center_axis',(1.92296268638356E-16,0.,-1.));
#11578=DIRECTION('ref_axis',(1.,0.,1.92296268638356E-16));
#11579=DIRECTION('',(1.,0.,1.92296268638356E-16));
#11580=DIRECTION('',(0.,-1.,0.));
#11581=DIRECTION('',(1.,0.,1.92296268638356E-16));
#11582=DIRECTION('center_axis',(-0.866025403784439,0.,-0.5));
#11583=DIRECTION('ref_axis',(0.5,0.,-0.866025403784439));
#11584=DIRECTION('',(0.5,0.,-0.866025403784439));
#11585=DIRECTION('',(0.,-1.,0.));
#11586=DIRECTION('',(0.5,0.,-0.866025403784438));
#11587=DIRECTION('center_axis',(-0.866025403784439,0.,0.5));
#11588=DIRECTION('ref_axis',(-0.5,0.,-0.866025403784439));
#11589=DIRECTION('',(-0.5,0.,-0.866025403784439));
#11590=DIRECTION('',(0.,-1.,0.));
#11591=DIRECTION('',(-0.5,0.,-0.866025403784439));
#11592=DIRECTION('center_axis',(-1.92296268638356E-16,0.,1.));
#11593=DIRECTION('ref_axis',(-1.,0.,-1.92296268638356E-16));
#11594=DIRECTION('',(-1.,0.,-1.92296268638356E-16));
#11595=DIRECTION('',(0.,-1.,0.));
#11596=DIRECTION('',(-1.,0.,-1.92296268638356E-16));
#11597=DIRECTION('center_axis',(0.866025403784439,0.,0.5));
#11598=DIRECTION('ref_axis',(-0.5,0.,0.866025403784439));
#11599=DIRECTION('',(-0.5,0.,0.866025403784439));
#11600=DIRECTION('',(-0.5,0.,0.866025403784439));
#11601=DIRECTION('center_axis',(0.,-1.,0.));
#11602=DIRECTION('ref_axis',(0.,0.,-1.));
#11603=DIRECTION('center_axis',(0.,1.,0.));
#11604=DIRECTION('ref_axis',(0.,0.,1.));
#11605=DIRECTION('center_axis',(0.,-1.,0.));
#11606=DIRECTION('ref_axis',(1.,0.,0.));
#11607=DIRECTION('center_axis',(0.,-1.,0.));
#11608=DIRECTION('ref_axis',(1.,0.,0.));
#11609=DIRECTION('center_axis',(0.,-1.,0.));
#11610=DIRECTION('ref_axis',(1.,0.,0.));
#11611=DIRECTION('',(0.707106781186547,0.707106781186548,8.65956056235493E-17));
#11612=DIRECTION('center_axis',(0.,-1.,0.));
#11613=DIRECTION('ref_axis',(1.,0.,0.));
#11614=DIRECTION('center_axis',(0.,1.,0.));
#11615=DIRECTION('ref_axis',(1.,0.,0.));
#11616=DIRECTION('',(0.,1.,0.));
#11617=DIRECTION('center_axis',(0.,1.,0.));
#11618=DIRECTION('ref_axis',(1.,0.,0.));
#11619=DIRECTION('center_axis',(0.,-1.,0.));
#11620=DIRECTION('ref_axis',(1.,0.,0.));
#11621=DIRECTION('',(-0.707106781186547,0.707106781186548,-8.65956056235493E-17));
#11622=DIRECTION('center_axis',(0.,-1.,0.));
#11623=DIRECTION('ref_axis',(0.,0.,-1.));
#14662=CARTESIAN_POINT('',(0.,0.,0.));
#14663=CARTESIAN_POINT('Origin',(0.0721687836487032,0.,-0.125));
#14664=CARTESIAN_POINT('',(0.0721687836487032,0.,-0.125));
#14665=CARTESIAN_POINT('',(0.144337567297406,0.,0.));
#14666=CARTESIAN_POINT('',(0.117710979560879,0.,-0.0461186027918559));
#14667=CARTESIAN_POINT('',(0.0721687836487032,-0.25,-0.125));
#14668=CARTESIAN_POINT('',(0.0721687836487032,0.,-0.125));
#14669=CARTESIAN_POINT('',(0.144337567297406,-0.25,0.));
#14670=CARTESIAN_POINT('',(0.144337567297406,-0.25,0.));
#14671=CARTESIAN_POINT('',(0.144337567297406,0.,0.));
#14672=CARTESIAN_POINT('Origin',(-0.0721687836487032,0.,-0.125));
#14673=CARTESIAN_POINT('',(-0.0721687836487032,0.,-0.125));
#14674=CARTESIAN_POINT('',(0.0739156081756484,0.,-0.125));
#14675=CARTESIAN_POINT('',(-0.0721687836487032,-0.25,-0.125));
#14676=CARTESIAN_POINT('',(-0.0721687836487032,0.,-0.125));
#14677=CARTESIAN_POINT('',(0.0721687836487032,-0.25,-0.125));
#14678=CARTESIAN_POINT('Origin',(-0.144337567297406,0.,-4.16333634234434E-17));
#14679=CARTESIAN_POINT('',(-0.144337567297406,0.,-1.76762539787485E-17));
#14680=CARTESIAN_POINT('',(-0.0987953713852306,0.,-0.0788813972081442));
#14681=CARTESIAN_POINT('',(-0.144337567297406,-0.25,-2.77555756156289E-17));
#14682=CARTESIAN_POINT('',(-0.144337567297406,0.,-1.76762539787485E-17));
#14683=CARTESIAN_POINT('',(-0.0721687836487032,-0.25,-0.125));
#14684=CARTESIAN_POINT('Origin',(-0.0721687836487033,0.,0.125));
#14685=CARTESIAN_POINT('',(-0.0721687836487033,0.,0.125));
#14686=CARTESIAN_POINT('',(-0.0627109795608791,0.,0.141381397208144));
#14687=CARTESIAN_POINT('',(-0.0721687836487033,-0.25,0.125));
#14688=CARTESIAN_POINT('',(-0.0721687836487033,0.,0.125));
#14689=CARTESIAN_POINT('',(-0.144337567297406,-0.25,-1.76762539787485E-17));
#14690=CARTESIAN_POINT('Origin',(0.0721687836487032,0.,0.125));
#14691=CARTESIAN_POINT('',(0.0721687836487032,0.,0.125));
#14692=CARTESIAN_POINT('',(0.146084391824352,0.,0.125));
#14693=CARTESIAN_POINT('',(0.0721687836487032,-0.25,0.125));
#14694=CARTESIAN_POINT('',(0.0721687836487032,0.,0.125));
#14695=CARTESIAN_POINT('',(-0.0721687836487033,-0.25,0.125));
#14696=CARTESIAN_POINT('Origin',(0.144337567297406,0.,0.));
#14697=CARTESIAN_POINT('',(0.153795371385231,0.,-0.0163813972081441));
#14698=CARTESIAN_POINT('',(0.0721687836487032,-0.25,0.125));
#14699=CARTESIAN_POINT('Origin',(0.,-0.25,0.));
#14700=CARTESIAN_POINT('Origin',(0.22,0.,0.));
#14701=CARTESIAN_POINT('',(-0.22,-8.67361737988404E-18,-2.69422295812418E-17));
#14702=CARTESIAN_POINT('Origin',(0.,0.,0.));
#14703=CARTESIAN_POINT('Origin',(0.,-0.015,0.));
#14704=CARTESIAN_POINT('',(-0.24505,-0.02505,-3.00099698131059E-17));
#14705=CARTESIAN_POINT('Origin',(0.,-0.02505,0.));
#14706=CARTESIAN_POINT('',(-0.235,-0.015,-2.87791997799628E-17));
#14707=CARTESIAN_POINT('Origin',(0.,-0.3775,0.));
#14708=CARTESIAN_POINT('',(-0.24505,-0.72995,3.00099698131059E-17));
#14709=CARTESIAN_POINT('Origin',(0.,-0.72995,0.));
#14710=CARTESIAN_POINT('',(-0.24505,-0.3775,-3.00099698131059E-17));
#14711=CARTESIAN_POINT('Origin',(0.,-0.7625,0.));
#14712=CARTESIAN_POINT('',(-0.175,-0.8,-2.14313189850787E-17));
#14713=CARTESIAN_POINT('Origin',(0.,-0.8,0.));
#14714=CARTESIAN_POINT('',(-0.2125,-0.7625,-2.60237444818813E-17));
#14715=CARTESIAN_POINT('Origin',(0.,-0.8,0.));
#14776=UNCERTAINTY_MEASURE_WITH_UNIT(LENGTH_MEASURE(0.001),#14823,
'DISTANCE_ACCURACY_VALUE',
'Maximum model space distance between geometric entities at asserted c
onnectivities');
#14777=UNCERTAINTY_MEASURE_WITH_UNIT(LENGTH_MEASURE(0.001),#14823,
'DISTANCE_ACCURACY_VALUE',
'Maximum model space distance between geometric entities at asserted c
onnectivities');
#14821=(
GEOMETRIC_REPRESENTATION_CONTEXT(3)
GLOBAL_UNCERTAINTY_ASSIGNED_CONTEXT((#14776))
GLOBAL_UNIT_ASSIGNED_CONTEXT((#14823,#14825,#14826))
REPRESENTATION_CONTEXT('','3D')
);
#14822=(
GEOMETRIC_REPRESENTATION_CONTEXT(3)
GLOBAL_UNCERTAINTY_ASSIGNED_CONTEXT((#14777))
GLOBAL_UNIT_ASSIGNED_CONTEXT((#14823,#14825,#14826))
REPRESENTATION_CONTEXT('','3D')
);
#14823=(
LENGTH_UNIT()
NAMED_UNIT(*)
SI_UNIT(.CENTI.,.METRE.)
);
#14825=(
NAMED_UNIT(*)
PLANE_ANGLE_UNIT()
SI_UNIT($,.RADIAN.)
);
#14826=(
NAMED_UNIT(*)
SI_UNIT($,.STERADIAN.)
SOLID_ANGLE_UNIT()
);
#14870=SHAPE_DEFINITION_REPRESENTATION(#14980,#15041);
#14980=PRODUCT_DEFINITION_SHAPE('',$,#15086);
#15041=SHAPE_REPRESENTATION('',(#9132),#14821);
#15042=PRODUCT_DEFINITION_CONTEXT('part definition',#15176,'design');
#15086=PRODUCT_DEFINITION('Socket Set Screw - M5x8',
'Socket Set Screw - M5x8',#15130,#15042);
#15130=PRODUCT_DEFINITION_FORMATION('',$,#15221);
#15176=APPLICATION_CONTEXT(
'Core Data for Automotive Mechanical Design Process');
#15177=PRODUCT_CONTEXT('part definition',#15176,'mechanical');
#15221=PRODUCT('Socket Set Screw - M5x8','Socket Set Screw - M5x8',
'Socket Set Screw - M5x8',(#15177));
#15285=COLOUR_RGB('Black',0.12,0.14,0.17);
#15286=FILL_AREA_STYLE_COLOUR('',#15285);
#15287=FILL_AREA_STYLE('',(#15286));
#15288=SURFACE_STYLE_FILL_AREA(#15287);
#15289=SURFACE_SIDE_STYLE('',(#15288));
#15290=SURFACE_STYLE_USAGE(.BOTH.,#15289);
#15291=PRESENTATION_STYLE_ASSIGNMENT((#15290));
ENDSEC;
END-ISO-10303-21;
